ISO-10303-21;
HEADER;
/* Generated by software containing ST-Developer
 * from STEP Tools, Inc. (www.steptools.com) 
 */

FILE_DESCRIPTION(
/* description */ ('PAT-091'),
/* implementation_level */ '2;1');

FILE_NAME(
/* name */ 'Screw retaining collar.step',
/* time_stamp */ '2026-10-27T15:34:44-07:00',
/* author */ (''),
/* organization */ (''),
/* preprocessor_version */ 'ST-DEVELOPER v20.2',
/* originating_system */ 'Autodesk Translation Framework v15.17.0.0',
/* authorisation */ '');

FILE_SCHEMA (('AUTOMOTIVE_DESIGN { 1 0 10303 214 3 1 1 }'));
ENDSEC;

DATA;
#10=MECHANICAL_DESIGN_GEOMETRIC_PRESENTATION_REPRESENTATION('',(#1091),#25100);
#858=SHAPE_REPRESENTATION_RELATIONSHIP('SRR','None',#25627,#968);
#968=ADVANCED_BREP_SHAPE_REPRESENTATION('',(#1212),#25097);
#1091=STYLED_ITEM('',(#26198),#1212);
#1212=MANIFOLD_SOLID_BREP('Body1',#13371);
#1633=FACE_BOUND('',#4106,.T.);
#1634=FACE_BOUND('',#4108,.T.);
#2056=PLANE('',#16430);
#2057=PLANE('',#16431);
#2867=FACE_OUTER_BOUND('',#4103,.T.);
#2868=FACE_OUTER_BOUND('',#4104,.T.);
#2869=FACE_OUTER_BOUND('',#4105,.T.);
#2870=FACE_OUTER_BOUND('',#4107,.T.);
#4103=EDGE_LOOP('',(#12032,#12033,#12034,#12035));
#4104=EDGE_LOOP('',(#12036,#12037,#12038,#12039));
#4105=EDGE_LOOP('',(#12040));
#4106=EDGE_LOOP('',(#12041));
#4107=EDGE_LOOP('',(#12042));
#4108=EDGE_LOOP('',(#12043));
#4857=LINE('',#24798,#5597);
#4858=LINE('',#24804,#5598);
#5597=VECTOR('',#20883,0.6);
#5598=VECTOR('',#20890,0.9);
#6369=CIRCLE('',#16425,0.6);
#6370=CIRCLE('',#16426,0.6);
#6371=CIRCLE('',#16428,0.9);
#6372=CIRCLE('',#16429,0.9);
#7407=VERTEX_POINT('',#24795);
#7408=VERTEX_POINT('',#24797);
#7409=VERTEX_POINT('',#24801);
#7410=VERTEX_POINT('',#24803);
#8951=EDGE_CURVE('',#7407,#7407,#6369,.T.);
#8952=EDGE_CURVE('',#7407,#7408,#4857,.T.);
#8953=EDGE_CURVE('',#7408,#7408,#6370,.T.);
#8954=EDGE_CURVE('',#7409,#7409,#6371,.T.);
#8955=EDGE_CURVE('',#7409,#7410,#4858,.T.);
#8956=EDGE_CURVE('',#7410,#7410,#6372,.T.);
#12032=ORIENTED_EDGE('',*,*,#8951,.F.);
#12033=ORIENTED_EDGE('',*,*,#8952,.T.);
#12034=ORIENTED_EDGE('',*,*,#8953,.T.);
#12035=ORIENTED_EDGE('',*,*,#8952,.F.);
#12036=ORIENTED_EDGE('',*,*,#8954,.F.);
#12037=ORIENTED_EDGE('',*,*,#8955,.T.);
#12038=ORIENTED_EDGE('',*,*,#8956,.T.);
#12039=ORIENTED_EDGE('',*,*,#8955,.F.);
#12040=ORIENTED_EDGE('',*,*,#8954,.T.);
#12041=ORIENTED_EDGE('',*,*,#8951,.T.);
#12042=ORIENTED_EDGE('',*,*,#8956,.F.);
#12043=ORIENTED_EDGE('',*,*,#8953,.F.);
#12423=CYLINDRICAL_SURFACE('',#16424,0.6);
#12424=CYLINDRICAL_SURFACE('',#16427,0.9);
#13234=ADVANCED_FACE('',(#2867),#12423,.F.);
#13235=ADVANCED_FACE('',(#2868),#12424,.T.);
#13236=ADVANCED_FACE('',(#2869,#1633),#2056,.T.);
#13237=ADVANCED_FACE('',(#2870,#1634),#2057,.F.);
#13371=CLOSED_SHELL('',(#13234,#13235,#13236,#13237));
#16423=AXIS2_PLACEMENT_3D('',#24793,#20877,#20878);
#16424=AXIS2_PLACEMENT_3D('',#24794,#20879,#20880);
#16425=AXIS2_PLACEMENT_3D('',#24796,#20881,#20882);
#16426=AXIS2_PLACEMENT_3D('',#24799,#20884,#20885);
#16427=AXIS2_PLACEMENT_3D('',#24800,#20886,#20887);
#16428=AXIS2_PLACEMENT_3D('',#24802,#20888,#20889);
#16429=AXIS2_PLACEMENT_3D('',#24805,#20891,#20892);
#16430=AXIS2_PLACEMENT_3D('',#24806,#20893,#20894);
#16431=AXIS2_PLACEMENT_3D('',#24807,#20895,#20896);
#20877=DIRECTION('axis',(0.,0.,1.));
#20878=DIRECTION('refdir',(1.,0.,0.));
#20879=DIRECTION('center_axis',(1.,0.,0.));
#20880=DIRECTION('ref_axis',(0.,0.,-1.));
#20881=DIRECTION('center_axis',(-1.,0.,0.));
#20882=DIRECTION('ref_axis',(0.,0.,-1.));
#20883=DIRECTION('',(-1.,0.,0.));
#20884=DIRECTION('center_axis',(-1.,0.,0.));
#20885=DIRECTION('ref_axis',(0.,0.,-1.));
#20886=DIRECTION('center_axis',(1.,0.,0.));
#20887=DIRECTION('ref_axis',(0.,0.,-1.));
#20888=DIRECTION('center_axis',(1.,0.,0.));
#20889=DIRECTION('ref_axis',(0.,0.,-1.));
#20890=DIRECTION('',(-1.,0.,0.));
#20891=DIRECTION('center_axis',(1.,0.,0.));
#20892=DIRECTION('ref_axis',(0.,0.,-1.));
#20893=DIRECTION('center_axis',(1.,0.,0.));
#20894=DIRECTION('ref_axis',(0.,0.,-1.));
#20895=DIRECTION('center_axis',(1.,0.,0.));
#20896=DIRECTION('ref_axis',(0.,0.,-1.));
#24793=CARTESIAN_POINT('',(0.,0.,0.));
#24794=CARTESIAN_POINT('Origin',(-1.5,0.,6.));
#24795=CARTESIAN_POINT('',(-1.3,-7.34788079488412E-17,6.6));
#24796=CARTESIAN_POINT('Origin',(-1.3,0.,6.));
#24797=CARTESIAN_POINT('',(-1.5,-7.34788079488412E-17,6.6));
#24798=CARTESIAN_POINT('',(-1.5,-7.34788079488412E-17,6.6));
#24799=CARTESIAN_POINT('Origin',(-1.5,0.,6.));
#24800=CARTESIAN_POINT('Origin',(-1.5,0.,6.));
#24801=CARTESIAN_POINT('',(-1.3,-1.10218211923262E-16,6.9));
#24802=CARTESIAN_POINT('Origin',(-1.3,0.,6.));
#24803=CARTESIAN_POINT('',(-1.5,-1.10218211923262E-16,6.9));
#24804=CARTESIAN_POINT('',(-1.5,-1.10218211923262E-16,6.9));
#24805=CARTESIAN_POINT('Origin',(-1.5,0.,6.));
#24806=CARTESIAN_POINT('Origin',(-1.3,0.,6.));
#24807=CARTESIAN_POINT('Origin',(-1.5,0.,6.));
#24976=UNCERTAINTY_MEASURE_WITH_UNIT(LENGTH_MEASURE(0.001),#25101,
'DISTANCE_ACCURACY_VALUE',
'Maximum model space distance between geometric entities at asserted c
onnectivities');
#24979=UNCERTAINTY_MEASURE_WITH_UNIT(LENGTH_MEASURE(0.001),#25101,
'DISTANCE_ACCURACY_VALUE',
'Maximum model space distance between geometric entities at asserted c
onnectivities');
#25097=(
GEOMETRIC_REPRESENTATION_CONTEXT(3)
GLOBAL_UNCERTAINTY_ASSIGNED_CONTEXT((#24976))
GLOBAL_UNIT_ASSIGNED_CONTEXT((#25101,#25103,#25104))
REPRESENTATION_CONTEXT('','3D')
);
#25100=(
GEOMETRIC_REPRESENTATION_CONTEXT(3)
GLOBAL_UNCERTAINTY_ASSIGNED_CONTEXT((#24979))
GLOBAL_UNIT_ASSIGNED_CONTEXT((#25101,#25103,#25104))
REPRESENTATION_CONTEXT('','3D')
);
#25101=(
LENGTH_UNIT()
NAMED_UNIT(*)
SI_UNIT(.CENTI.,.METRE.)
);
#25103=(
NAMED_UNIT(*)
PLANE_ANGLE_UNIT()
SI_UNIT($,.RADIAN.)
);
#25104=(
NAMED_UNIT(*)
SI_UNIT($,.STERADIAN.)
SOLID_ANGLE_UNIT()
);
#25222=SHAPE_DEFINITION_REPRESENTATION(#25494,#25627);
#25494=PRODUCT_DEFINITION_SHAPE('',$,#25748);
#25627=SHAPE_REPRESENTATION('',(#16423),#25097);
#25630=PRODUCT_DEFINITION_CONTEXT('part definition',#25992,'design');
#25748=PRODUCT_DEFINITION('Screw retaining collar',
'Screw retaining collar',#25868,#25630);
#25868=PRODUCT_DEFINITION_FORMATION('',$,#26111);
#25992=APPLICATION_CONTEXT(
'Core Data for Automotive Mechanical Design Process');
#25993=PRODUCT_CONTEXT('part definition',#25992,'mechanical');
#26111=PRODUCT('Screw retaining collar','Screw retaining collar',
'Screw retaining collar',(#25993));
#26192=COLOUR_RGB('Black',0.12,0.14,0.17);
#26193=FILL_AREA_STYLE_COLOUR('',#26192);
#26194=FILL_AREA_STYLE('',(#26193));
#26195=SURFACE_STYLE_FILL_AREA(#26194);
#26196=SURFACE_SIDE_STYLE('',(#26195));
#26197=SURFACE_STYLE_USAGE(.BOTH.,#26196);
#26198=PRESENTATION_STYLE_ASSIGNMENT((#26197));
ENDSEC;
END-ISO-10303-21;
